ISO-10303-21;
HEADER;
/* Generated by software containing ST-Developer
 * from STEP Tools, Inc. (www.steptools.com) 
 */

FILE_DESCRIPTION(
/* description */ ('Bin tilter linkage'),
/* implementation_level */ '2;1');

FILE_NAME(
/* name */ 'M4 short cap screw (16).step',
/* time_stamp */ '2026-10-28T03:26:24-07:00',
/* author */ (''),
/* organization */ (''),
/* preprocessor_version */ 'ST-DEVELOPER v20.2',
/* originating_system */ 'Autodesk Translation Framework v15.17.0.0',
/* authorisation */ '');

FILE_SCHEMA (('AUTOMOTIVE_DESIGN { 1 0 10303 214 3 1 1 }'));
ENDSEC;

DATA;
#10=MECHANICAL_DESIGN_GEOMETRIC_PRESENTATION_REPRESENTATION('',(#915),#23728);
#703=SHAPE_REPRESENTATION_RELATIONSHIP('SRR','None',#24169,#809);
#809=ADVANCED_BREP_SHAPE_REPRESENTATION('',(#1028),#23669);
#915=STYLED_ITEM('',(#24772),#1028);
#1028=MANIFOLD_SOLID_BREP('Body1',#12446);
#1340=FACE_BOUND('',#3322,.T.);
#1683=PLANE('',#14551);
#1684=PLANE('',#14556);
#1685=PLANE('',#14559);
#2291=FACE_OUTER_BOUND('',#3321,.T.);
#2292=FACE_OUTER_BOUND('',#3323,.T.);
#2293=FACE_OUTER_BOUND('',#3324,.T.);
#2294=FACE_OUTER_BOUND('',#3325,.T.);
#2295=FACE_OUTER_BOUND('',#3326,.T.);
#3321=EDGE_LOOP('',(#9913));
#3322=EDGE_LOOP('',(#9914));
#3323=EDGE_LOOP('',(#9915,#9916,#9917,#9918));
#3324=EDGE_LOOP('',(#9919));
#3325=EDGE_LOOP('',(#9920,#9921,#9922,#9923));
#3326=EDGE_LOOP('',(#9924));
#4203=LINE('',#21493,#4878);
#4204=LINE('',#21499,#4879);
#4878=VECTOR('',#17586,0.350000000000001);
#4879=VECTOR('',#17595,0.199999999999999);
#5615=CIRCLE('',#14552,0.350000000000001);
#5616=CIRCLE('',#14553,0.199999999999999);
#5617=CIRCLE('',#14555,0.350000000000001);
#5618=CIRCLE('',#14558,0.199999999999999);
#6469=VERTEX_POINT('',#21487);
#6470=VERTEX_POINT('',#21489);
#6471=VERTEX_POINT('',#21492);
#6472=VERTEX_POINT('',#21497);
#7696=EDGE_CURVE('',#6469,#6469,#5615,.T.);
#7697=EDGE_CURVE('',#6470,#6470,#5616,.T.);
#7698=EDGE_CURVE('',#6469,#6471,#4203,.T.);
#7699=EDGE_CURVE('',#6471,#6471,#5617,.T.);
#7700=EDGE_CURVE('',#6472,#6472,#5618,.T.);
#7701=EDGE_CURVE('',#6472,#6470,#4204,.T.);
#9913=ORIENTED_EDGE('',*,*,#7696,.T.);
#9914=ORIENTED_EDGE('',*,*,#7697,.F.);
#9915=ORIENTED_EDGE('',*,*,#7696,.F.);
#9916=ORIENTED_EDGE('',*,*,#7698,.T.);
#9917=ORIENTED_EDGE('',*,*,#7699,.T.);
#9918=ORIENTED_EDGE('',*,*,#7698,.F.);
#9919=ORIENTED_EDGE('',*,*,#7699,.F.);
#9920=ORIENTED_EDGE('',*,*,#7700,.F.);
#9921=ORIENTED_EDGE('',*,*,#7701,.T.);
#9922=ORIENTED_EDGE('',*,*,#7697,.T.);
#9923=ORIENTED_EDGE('',*,*,#7701,.F.);
#9924=ORIENTED_EDGE('',*,*,#7700,.T.);
#11473=CYLINDRICAL_SURFACE('',#14554,0.350000000000001);
#11474=CYLINDRICAL_SURFACE('',#14557,0.199999999999999);
#12016=ADVANCED_FACE('',(#2291,#1340),#1683,.T.);
#12017=ADVANCED_FACE('',(#2292),#11473,.T.);
#12018=ADVANCED_FACE('',(#2293),#1684,.F.);
#12019=ADVANCED_FACE('',(#2294),#11474,.T.);
#12020=ADVANCED_FACE('',(#2295),#1685,.T.);
#12446=CLOSED_SHELL('',(#12016,#12017,#12018,#12019,#12020));
#14550=AXIS2_PLACEMENT_3D('',#21485,#17576,#17577);
#14551=AXIS2_PLACEMENT_3D('',#21486,#17578,#17579);
#14552=AXIS2_PLACEMENT_3D('',#21488,#17580,#17581);
#14553=AXIS2_PLACEMENT_3D('',#21490,#17582,#17583);
#14554=AXIS2_PLACEMENT_3D('',#21491,#17584,#17585);
#14555=AXIS2_PLACEMENT_3D('',#21494,#17587,#17588);
#14556=AXIS2_PLACEMENT_3D('',#21495,#17589,#17590);
#14557=AXIS2_PLACEMENT_3D('',#21496,#17591,#17592);
#14558=AXIS2_PLACEMENT_3D('',#21498,#17593,#17594);
#14559=AXIS2_PLACEMENT_3D('',#21500,#17596,#17597);
#17576=DIRECTION('axis',(0.,0.,1.));
#17577=DIRECTION('refdir',(1.,0.,0.));
#17578=DIRECTION('center_axis',(0.,1.,0.));
#17579=DIRECTION('ref_axis',(1.,0.,0.));
#17580=DIRECTION('center_axis',(0.,1.,0.));
#17581=DIRECTION('ref_axis',(1.,0.,0.));
#17582=DIRECTION('center_axis',(0.,1.,0.));
#17583=DIRECTION('ref_axis',(1.,0.,0.));
#17584=DIRECTION('center_axis',(0.,1.,0.));
#17585=DIRECTION('ref_axis',(1.,0.,0.));
#17586=DIRECTION('',(0.,-1.,0.));
#17587=DIRECTION('center_axis',(0.,1.,0.));
#17588=DIRECTION('ref_axis',(1.,0.,0.));
#17589=DIRECTION('center_axis',(0.,1.,0.));
#17590=DIRECTION('ref_axis',(1.,0.,0.));
#17591=DIRECTION('center_axis',(0.,1.,0.));
#17592=DIRECTION('ref_axis',(1.,0.,0.));
#17593=DIRECTION('center_axis',(0.,1.,0.));
#17594=DIRECTION('ref_axis',(1.,0.,0.));
#17595=DIRECTION('',(0.,-1.,0.));
#17596=DIRECTION('center_axis',(0.,1.,0.));
#17597=DIRECTION('ref_axis',(1.,0.,0.));
#21485=CARTESIAN_POINT('',(0.,0.,0.));
#21486=CARTESIAN_POINT('Origin',(19.3081475451951,-0.8,16.3081475451951));
#21487=CARTESIAN_POINT('',(18.9581475451951,-0.8,16.3081475451951));
#21488=CARTESIAN_POINT('Origin',(19.3081475451951,-0.8,16.3081475451951));
#21489=CARTESIAN_POINT('',(19.1081475451951,-0.8,16.3081475451951));
#21490=CARTESIAN_POINT('Origin',(19.3081475451951,-0.8,16.3081475451951));
#21491=CARTESIAN_POINT('Origin',(19.3081475451951,-1.2,16.3081475451951));
#21492=CARTESIAN_POINT('',(18.9581475451951,-1.2,16.3081475451951));
#21493=CARTESIAN_POINT('',(18.9581475451951,-1.2,16.3081475451951));
#21494=CARTESIAN_POINT('Origin',(19.3081475451951,-1.2,16.3081475451951));
#21495=CARTESIAN_POINT('Origin',(19.3081475451951,-1.2,16.3081475451951));
#21496=CARTESIAN_POINT('Origin',(19.3081475451951,-0.8,16.3081475451951));
#21497=CARTESIAN_POINT('',(19.1081475451951,-0.1,16.3081475451951));
#21498=CARTESIAN_POINT('Origin',(19.3081475451951,-0.1,16.3081475451951));
#21499=CARTESIAN_POINT('',(19.1081475451951,-0.8,16.3081475451951));
#21500=CARTESIAN_POINT('Origin',(19.3081475451951,-0.1,16.3081475451951));
#23552=UNCERTAINTY_MEASURE_WITH_UNIT(LENGTH_MEASURE(0.001),#23729,
'DISTANCE_ACCURACY_VALUE',
'Maximum model space distance between geometric entities at asserted c
onnectivities');
#23611=UNCERTAINTY_MEASURE_WITH_UNIT(LENGTH_MEASURE(0.001),#23729,
'DISTANCE_ACCURACY_VALUE',
'Maximum model space distance between geometric entities at asserted c
onnectivities');
#23669=(
GEOMETRIC_REPRESENTATION_CONTEXT(3)
GLOBAL_UNCERTAINTY_ASSIGNED_CONTEXT((#23552))
GLOBAL_UNIT_ASSIGNED_CONTEXT((#23729,#23731,#23732))
REPRESENTATION_CONTEXT('','3D')
);
#23728=(
GEOMETRIC_REPRESENTATION_CONTEXT(3)
GLOBAL_UNCERTAINTY_ASSIGNED_CONTEXT((#23611))
GLOBAL_UNIT_ASSIGNED_CONTEXT((#23729,#23731,#23732))
REPRESENTATION_CONTEXT('','3D')
);
#23729=(
LENGTH_UNIT()
NAMED_UNIT(*)
SI_UNIT(.CENTI.,.METRE.)
);
#23731=(
NAMED_UNIT(*)
PLANE_ANGLE_UNIT()
SI_UNIT($,.RADIAN.)
);
#23732=(
NAMED_UNIT(*)
SI_UNIT($,.STERADIAN.)
SOLID_ANGLE_UNIT()
);
#23790=SHAPE_DEFINITION_REPRESENTATION(#23906,#24169);
#23906=PRODUCT_DEFINITION_SHAPE('',$,#24286);
#24169=SHAPE_REPRESENTATION('',(#14550),#23669);
#24228=PRODUCT_DEFINITION_CONTEXT('part definition',#24578,'design');
#24286=PRODUCT_DEFINITION('M4 short cap screw (16)',
'M4 short cap screw (16)',#24402,#24228);
#24402=PRODUCT_DEFINITION_FORMATION('',$,#24637);
#24578=APPLICATION_CONTEXT(
'Core Data for Automotive Mechanical Design Process');
#24579=PRODUCT_CONTEXT('part definition',#24578,'mechanical');
#24637=PRODUCT('M4 short cap screw (16)','M4 short cap screw (16)',
'M4 short cap screw (16)',(#24579));
#24766=COLOUR_RGB('Black',0.12,0.14,0.17);
#24767=FILL_AREA_STYLE_COLOUR('',#24766);
#24768=FILL_AREA_STYLE('',(#24767));
#24769=SURFACE_STYLE_FILL_AREA(#24768);
#24770=SURFACE_SIDE_STYLE('',(#24769));
#24771=SURFACE_STYLE_USAGE(.BOTH.,#24770);
#24772=PRESENTATION_STYLE_ASSIGNMENT((#24771));
ENDSEC;
END-ISO-10303-21;
